ISO-10303-21;
HEADER;
/* Generated by software containing ST-Developer
 * from STEP Tools, Inc. (www.steptools.com) 
 */

FILE_DESCRIPTION(
/* description */ ('Bin tilter linkage'),
/* implementation_level */ '2;1');

FILE_NAME(
/* name */ 'M4 short cap screw (19).step',
/* time_stamp */ '2026-10-28T03:26:24-07:00',
/* author */ (''),
/* organization */ (''),
/* preprocessor_version */ 'ST-DEVELOPER v20.2',
/* originating_system */ 'Autodesk Translation Framework v15.17.0.0',
/* authorisation */ '');

FILE_SCHEMA (('AUTOMOTIVE_DESIGN { 1 0 10303 214 3 1 1 }'));
ENDSEC;

DATA;
#10=MECHANICAL_DESIGN_GEOMETRIC_PRESENTATION_REPRESENTATION('',(#918),#23728);
#706=SHAPE_REPRESENTATION_RELATIONSHIP('SRR','None',#24172,#812);
#812=ADVANCED_BREP_SHAPE_REPRESENTATION('',(#1031),#23672);
#918=STYLED_ITEM('',(#24772),#1031);
#1031=MANIFOLD_SOLID_BREP('Body1',#12449);
#1343=FACE_BOUND('',#3340,.T.);
#1692=PLANE('',#14581);
#1693=PLANE('',#14586);
#1694=PLANE('',#14589);
#2306=FACE_OUTER_BOUND('',#3339,.T.);
#2307=FACE_OUTER_BOUND('',#3341,.T.);
#2308=FACE_OUTER_BOUND('',#3342,.T.);
#2309=FACE_OUTER_BOUND('',#3343,.T.);
#2310=FACE_OUTER_BOUND('',#3344,.T.);
#3339=EDGE_LOOP('',(#9949));
#3340=EDGE_LOOP('',(#9950));
#3341=EDGE_LOOP('',(#9951,#9952,#9953,#9954));
#3342=EDGE_LOOP('',(#9955));
#3343=EDGE_LOOP('',(#9956,#9957,#9958,#9959));
#3344=EDGE_LOOP('',(#9960));
#4209=LINE('',#21541,#4884);
#4210=LINE('',#21547,#4885);
#4884=VECTOR('',#17652,0.350000000000001);
#4885=VECTOR('',#17661,0.199999999999999);
#5627=CIRCLE('',#14582,0.350000000000001);
#5628=CIRCLE('',#14583,0.199999999999999);
#5629=CIRCLE('',#14585,0.350000000000001);
#5630=CIRCLE('',#14588,0.199999999999999);
#6481=VERTEX_POINT('',#21535);
#6482=VERTEX_POINT('',#21537);
#6483=VERTEX_POINT('',#21540);
#6484=VERTEX_POINT('',#21545);
#7714=EDGE_CURVE('',#6481,#6481,#5627,.T.);
#7715=EDGE_CURVE('',#6482,#6482,#5628,.T.);
#7716=EDGE_CURVE('',#6481,#6483,#4209,.T.);
#7717=EDGE_CURVE('',#6483,#6483,#5629,.T.);
#7718=EDGE_CURVE('',#6484,#6484,#5630,.T.);
#7719=EDGE_CURVE('',#6484,#6482,#4210,.T.);
#9949=ORIENTED_EDGE('',*,*,#7714,.T.);
#9950=ORIENTED_EDGE('',*,*,#7715,.F.);
#9951=ORIENTED_EDGE('',*,*,#7714,.F.);
#9952=ORIENTED_EDGE('',*,*,#7716,.T.);
#9953=ORIENTED_EDGE('',*,*,#7717,.T.);
#9954=ORIENTED_EDGE('',*,*,#7716,.F.);
#9955=ORIENTED_EDGE('',*,*,#7717,.F.);
#9956=ORIENTED_EDGE('',*,*,#7718,.F.);
#9957=ORIENTED_EDGE('',*,*,#7719,.T.);
#9958=ORIENTED_EDGE('',*,*,#7715,.T.);
#9959=ORIENTED_EDGE('',*,*,#7719,.F.);
#9960=ORIENTED_EDGE('',*,*,#7718,.T.);
#11479=CYLINDRICAL_SURFACE('',#14584,0.350000000000001);
#11480=CYLINDRICAL_SURFACE('',#14587,0.199999999999999);
#12031=ADVANCED_FACE('',(#2306,#1343),#1692,.T.);
#12032=ADVANCED_FACE('',(#2307),#11479,.T.);
#12033=ADVANCED_FACE('',(#2308),#1693,.F.);
#12034=ADVANCED_FACE('',(#2309),#11480,.T.);
#12035=ADVANCED_FACE('',(#2310),#1694,.T.);
#12449=CLOSED_SHELL('',(#12031,#12032,#12033,#12034,#12035));
#14580=AXIS2_PLACEMENT_3D('',#21533,#17642,#17643);
#14581=AXIS2_PLACEMENT_3D('',#21534,#17644,#17645);
#14582=AXIS2_PLACEMENT_3D('',#21536,#17646,#17647);
#14583=AXIS2_PLACEMENT_3D('',#21538,#17648,#17649);
#14584=AXIS2_PLACEMENT_3D('',#21539,#17650,#17651);
#14585=AXIS2_PLACEMENT_3D('',#21542,#17653,#17654);
#14586=AXIS2_PLACEMENT_3D('',#21543,#17655,#17656);
#14587=AXIS2_PLACEMENT_3D('',#21544,#17657,#17658);
#14588=AXIS2_PLACEMENT_3D('',#21546,#17659,#17660);
#14589=AXIS2_PLACEMENT_3D('',#21548,#17662,#17663);
#17642=DIRECTION('axis',(0.,0.,1.));
#17643=DIRECTION('refdir',(1.,0.,0.));
#17644=DIRECTION('center_axis',(0.,1.,0.));
#17645=DIRECTION('ref_axis',(1.,0.,0.));
#17646=DIRECTION('center_axis',(0.,1.,0.));
#17647=DIRECTION('ref_axis',(1.,0.,0.));
#17648=DIRECTION('center_axis',(0.,1.,0.));
#17649=DIRECTION('ref_axis',(1.,0.,0.));
#17650=DIRECTION('center_axis',(0.,1.,0.));
#17651=DIRECTION('ref_axis',(1.,0.,0.));
#17652=DIRECTION('',(0.,-1.,0.));
#17653=DIRECTION('center_axis',(0.,1.,0.));
#17654=DIRECTION('ref_axis',(1.,0.,0.));
#17655=DIRECTION('center_axis',(0.,1.,0.));
#17656=DIRECTION('ref_axis',(1.,0.,0.));
#17657=DIRECTION('center_axis',(0.,1.,0.));
#17658=DIRECTION('ref_axis',(1.,0.,0.));
#17659=DIRECTION('center_axis',(0.,1.,0.));
#17660=DIRECTION('ref_axis',(1.,0.,0.));
#17661=DIRECTION('',(0.,-1.,0.));
#17662=DIRECTION('center_axis',(0.,1.,0.));
#17663=DIRECTION('ref_axis',(1.,0.,0.));
#21533=CARTESIAN_POINT('',(0.,0.,0.));
#21534=CARTESIAN_POINT('Origin',(19.3081475451951,-0.8,13.6918524548049));
#21535=CARTESIAN_POINT('',(18.9581475451951,-0.8,13.6918524548049));
#21536=CARTESIAN_POINT('Origin',(19.3081475451951,-0.8,13.6918524548049));
#21537=CARTESIAN_POINT('',(19.1081475451951,-0.8,13.6918524548049));
#21538=CARTESIAN_POINT('Origin',(19.3081475451951,-0.8,13.6918524548049));
#21539=CARTESIAN_POINT('Origin',(19.3081475451951,-1.2,13.6918524548049));
#21540=CARTESIAN_POINT('',(18.9581475451951,-1.2,13.6918524548049));
#21541=CARTESIAN_POINT('',(18.9581475451951,-1.2,13.6918524548049));
#21542=CARTESIAN_POINT('Origin',(19.3081475451951,-1.2,13.6918524548049));
#21543=CARTESIAN_POINT('Origin',(19.3081475451951,-1.2,13.6918524548049));
#21544=CARTESIAN_POINT('Origin',(19.3081475451951,-0.8,13.6918524548049));
#21545=CARTESIAN_POINT('',(19.1081475451951,-0.1,13.6918524548049));
#21546=CARTESIAN_POINT('Origin',(19.3081475451951,-0.1,13.6918524548049));
#21547=CARTESIAN_POINT('',(19.1081475451951,-0.8,13.6918524548049));
#21548=CARTESIAN_POINT('Origin',(19.3081475451951,-0.1,13.6918524548049));
#23555=UNCERTAINTY_MEASURE_WITH_UNIT(LENGTH_MEASURE(0.001),#23729,
'DISTANCE_ACCURACY_VALUE',
'Maximum model space distance between geometric entities at asserted c
onnectivities');
#23611=UNCERTAINTY_MEASURE_WITH_UNIT(LENGTH_MEASURE(0.001),#23729,
'DISTANCE_ACCURACY_VALUE',
'Maximum model space distance between geometric entities at asserted c
onnectivities');
#23672=(
GEOMETRIC_REPRESENTATION_CONTEXT(3)
GLOBAL_UNCERTAINTY_ASSIGNED_CONTEXT((#23555))
GLOBAL_UNIT_ASSIGNED_CONTEXT((#23729,#23731,#23732))
REPRESENTATION_CONTEXT('','3D')
);
#23728=(
GEOMETRIC_REPRESENTATION_CONTEXT(3)
GLOBAL_UNCERTAINTY_ASSIGNED_CONTEXT((#23611))
GLOBAL_UNIT_ASSIGNED_CONTEXT((#23729,#23731,#23732))
REPRESENTATION_CONTEXT('','3D')
);
#23729=(
LENGTH_UNIT()
NAMED_UNIT(*)
SI_UNIT(.CENTI.,.METRE.)
);
#23731=(
NAMED_UNIT(*)
PLANE_ANGLE_UNIT()
SI_UNIT($,.RADIAN.)
);
#23732=(
NAMED_UNIT(*)
SI_UNIT($,.STERADIAN.)
SOLID_ANGLE_UNIT()
);
#23793=SHAPE_DEFINITION_REPRESENTATION(#23909,#24172);
#23909=PRODUCT_DEFINITION_SHAPE('',$,#24289);
#24172=SHAPE_REPRESENTATION('',(#14580),#23672);
#24228=PRODUCT_DEFINITION_CONTEXT('part definition',#24578,'design');
#24289=PRODUCT_DEFINITION('M4 short cap screw (19)',
'M4 short cap screw (19)',#24405,#24228);
#24405=PRODUCT_DEFINITION_FORMATION('',$,#24640);
#24578=APPLICATION_CONTEXT(
'Core Data for Automotive Mechanical Design Process');
#24579=PRODUCT_CONTEXT('part definition',#24578,'mechanical');
#24640=PRODUCT('M4 short cap screw (19)','M4 short cap screw (19)',
'M4 short cap screw (19)',(#24579));
#24766=COLOUR_RGB('Black',0.12,0.14,0.17);
#24767=FILL_AREA_STYLE_COLOUR('',#24766);
#24768=FILL_AREA_STYLE('',(#24767));
#24769=SURFACE_STYLE_FILL_AREA(#24768);
#24770=SURFACE_SIDE_STYLE('',(#24769));
#24771=SURFACE_STYLE_USAGE(.BOTH.,#24770);
#24772=PRESENTATION_STYLE_ASSIGNMENT((#24771));
ENDSEC;
END-ISO-10303-21;
